ISO-10303-21;
HEADER;
/* Generated by software containing ST-Developer
 * from STEP Tools, Inc. (www.steptools.com) 
 */

FILE_DESCRIPTION(
/* description */ ('PAT-065'),
/* implementation_level */ '2;1');

FILE_NAME(
/* name */ 'Slot Nut - M5 for 20 mm Extrusion.step',
/* time_stamp */ '2026-10-28T22:09:22-07:00',
/* author */ (''),
/* organization */ (''),
/* preprocessor_version */ 'ST-DEVELOPER v20.2',
/* originating_system */ 'Autodesk Translation Framework v15.17.0.0',
/* authorisation */ '');

FILE_SCHEMA (('AUTOMOTIVE_DESIGN { 1 0 10303 214 3 1 1 }'));
ENDSEC;

DATA;
#10=MECHANICAL_DESIGN_GEOMETRIC_PRESENTATION_REPRESENTATION('',(#166),#5502);
#133=ELLIPSE('',#3550,0.707106781186548,0.5);
#134=ELLIPSE('',#3555,0.707106781186548,0.5);
#135=ELLIPSE('',#3562,0.299389011154384,0.2117);
#136=ELLIPSE('',#3564,0.299389011154384,0.2117);
#137=ELLIPSE('',#3566,0.299389011154384,0.2117);
#146=SHAPE_REPRESENTATION_RELATIONSHIP('SRR','None',#5564,#156);
#156=ADVANCED_BREP_SHAPE_REPRESENTATION('',(#175),#5500);
#166=STYLED_ITEM('',(#5701),#175);
#175=MANIFOLD_SOLID_BREP('Body1',#3214);
#314=PLANE('',#3557);
#315=PLANE('',#3558);
#316=PLANE('',#3559);
#317=PLANE('',#3560);
#318=PLANE('',#3561);
#319=PLANE('',#3563);
#320=PLANE('',#3565);
#321=PLANE('',#3571);
#322=PLANE('',#3572);
#323=PLANE('',#3573);
#324=PLANE('',#3574);
#325=PLANE('',#3575);
#326=PLANE('',#3576);
#481=FACE_OUTER_BOUND('',#677,.T.);
#482=FACE_OUTER_BOUND('',#678,.T.);
#483=FACE_OUTER_BOUND('',#679,.T.);
#484=FACE_OUTER_BOUND('',#680,.T.);
#485=FACE_OUTER_BOUND('',#681,.T.);
#486=FACE_OUTER_BOUND('',#682,.T.);
#487=FACE_OUTER_BOUND('',#683,.T.);
#488=FACE_OUTER_BOUND('',#684,.T.);
#489=FACE_OUTER_BOUND('',#685,.T.);
#490=FACE_OUTER_BOUND('',#686,.T.);
#491=FACE_OUTER_BOUND('',#687,.T.);
#492=FACE_OUTER_BOUND('',#688,.T.);
#493=FACE_OUTER_BOUND('',#689,.T.);
#494=FACE_OUTER_BOUND('',#690,.T.);
#495=FACE_OUTER_BOUND('',#691,.T.);
#496=FACE_OUTER_BOUND('',#692,.T.);
#677=EDGE_LOOP('',(#2864,#2865,#2866,#2867));
#678=EDGE_LOOP('',(#2868,#2869,#2870,#2871));
#679=EDGE_LOOP('',(#2872,#2873,#2874,#2875));
#680=EDGE_LOOP('',(#2876,#2877,#2878,#2879));
#681=EDGE_LOOP('',(#2880,#2881,#2882,#2883));
#682=EDGE_LOOP('',(#2884,#2885,#2886,#2887));
#683=EDGE_LOOP('',(#2888,#2889,#2890,#2891,#2892,#2893));
#684=EDGE_LOOP('',(#2894,#2895,#2896,#2897,#2898,#2899));
#685=EDGE_LOOP('',(#2900,#2901,#2902,#2903,#2904,#2905));
#686=EDGE_LOOP('',(#2906,#2907,#2908,#2909,#2910,#2911,#2912,#2913));
#687=EDGE_LOOP('',(#2914,#2915,#2916,#2917));
#688=EDGE_LOOP('',(#2918,#2919,#2920,#2921));
#689=EDGE_LOOP('',(#2922,#2923,#2924,#2925,#2926,#2927));
#690=EDGE_LOOP('',(#2928,#2929,#2930,#2931));
#691=EDGE_LOOP('',(#2932,#2933,#2934,#2935,#2936,#2937));
#692=EDGE_LOOP('',(#2938,#2939,#2940,#2941,#2942,#2943,#2944,#2945,#2946,
#2947));
#988=LINE('',#5317,#1319);
#989=LINE('',#5322,#1320);
#990=LINE('',#5330,#1321);
#991=LINE('',#5332,#1322);
#992=LINE('',#5333,#1323);
#993=LINE('',#5336,#1324);
#994=LINE('',#5338,#1325);
#995=LINE('',#5339,#1326);
#996=LINE('',#5342,#1327);
#997=LINE('',#5344,#1328);
#998=LINE('',#5345,#1329);
#999=LINE('',#5348,#1330);
#1000=LINE('',#5350,#1331);
#1001=LINE('',#5351,#1332);
#1002=LINE('',#5354,#1333);
#1003=LINE('',#5356,#1334);
#1004=LINE('',#5362,#1335);
#1005=LINE('',#5363,#1336);
#1006=LINE('',#5367,#1337);
#1007=LINE('',#5369,#1338);
#1008=LINE('',#5371,#1339);
#1009=LINE('',#5373,#1340);
#1010=LINE('',#5376,#1341);
#1011=LINE('',#5382,#1342);
#1012=LINE('',#5384,#1343);
#1013=LINE('',#5387,#1344);
#1014=LINE('',#5388,#1345);
#1015=LINE('',#5391,#1346);
#1016=LINE('',#5392,#1347);
#1017=LINE('',#5394,#1348);
#1319=VECTOR('',#4347,1.);
#1320=VECTOR('',#4352,1.);
#1321=VECTOR('',#4361,1.);
#1322=VECTOR('',#4362,1.);
#1323=VECTOR('',#4363,1.);
#1324=VECTOR('',#4366,1.);
#1325=VECTOR('',#4367,1.);
#1326=VECTOR('',#4368,1.);
#1327=VECTOR('',#4371,1.);
#1328=VECTOR('',#4372,1.);
#1329=VECTOR('',#4373,1.);
#1330=VECTOR('',#4376,1.);
#1331=VECTOR('',#4377,1.);
#1332=VECTOR('',#4378,1.);
#1333=VECTOR('',#4381,1.);
#1334=VECTOR('',#4382,1.);
#1335=VECTOR('',#4389,1.);
#1336=VECTOR('',#4390,1.);
#1337=VECTOR('',#4393,1.);
#1338=VECTOR('',#4394,1.);
#1339=VECTOR('',#4395,1.);
#1340=VECTOR('',#4396,1.);
#1341=VECTOR('',#4399,1.);
#1342=VECTOR('',#4410,1.);
#1343=VECTOR('',#4413,1.);
#1344=VECTOR('',#4416,1.);
#1345=VECTOR('',#4417,1.);
#1346=VECTOR('',#4420,1.);
#1347=VECTOR('',#4421,1.);
#1348=VECTOR('',#4424,1.);
#1431=CIRCLE('',#3551,0.5);
#1432=CIRCLE('',#3552,0.5);
#1433=CIRCLE('',#3554,0.5);
#1434=CIRCLE('',#3556,0.5);
#1435=CIRCLE('',#3568,0.2117);
#1436=CIRCLE('',#3569,0.2117);
#1437=CIRCLE('',#3570,0.2117);
#1680=VERTEX_POINT('',#5311);
#1681=VERTEX_POINT('',#5312);
#1682=VERTEX_POINT('',#5314);
#1683=VERTEX_POINT('',#5316);
#1684=VERTEX_POINT('',#5320);
#1685=VERTEX_POINT('',#5321);
#1686=VERTEX_POINT('',#5323);
#1687=VERTEX_POINT('',#5325);
#1688=VERTEX_POINT('',#5329);
#1689=VERTEX_POINT('',#5331);
#1690=VERTEX_POINT('',#5335);
#1691=VERTEX_POINT('',#5337);
#1692=VERTEX_POINT('',#5341);
#1693=VERTEX_POINT('',#5343);
#1694=VERTEX_POINT('',#5347);
#1695=VERTEX_POINT('',#5349);
#1696=VERTEX_POINT('',#5353);
#1697=VERTEX_POINT('',#5355);
#1698=VERTEX_POINT('',#5359);
#1699=VERTEX_POINT('',#5361);
#1700=VERTEX_POINT('',#5365);
#1701=VERTEX_POINT('',#5366);
#1702=VERTEX_POINT('',#5368);
#1703=VERTEX_POINT('',#5370);
#1704=VERTEX_POINT('',#5372);
#1705=VERTEX_POINT('',#5374);
#1706=VERTEX_POINT('',#5386);
#1707=VERTEX_POINT('',#5390);
#2082=EDGE_CURVE('',#1680,#1681,#133,.T.);
#2083=EDGE_CURVE('',#1682,#1680,#1431,.T.);
#2084=EDGE_CURVE('',#1683,#1682,#988,.T.);
#2085=EDGE_CURVE('',#1681,#1683,#1432,.T.);
#2086=EDGE_CURVE('',#1684,#1685,#989,.T.);
#2087=EDGE_CURVE('',#1686,#1684,#1433,.T.);
#2088=EDGE_CURVE('',#1687,#1686,#134,.T.);
#2089=EDGE_CURVE('',#1685,#1687,#1434,.T.);
#2090=EDGE_CURVE('',#1688,#1680,#990,.T.);
#2091=EDGE_CURVE('',#1689,#1688,#991,.T.);
#2092=EDGE_CURVE('',#1682,#1689,#992,.T.);
#2093=EDGE_CURVE('',#1690,#1684,#993,.T.);
#2094=EDGE_CURVE('',#1691,#1690,#994,.T.);
#2095=EDGE_CURVE('',#1686,#1691,#995,.T.);
#2096=EDGE_CURVE('',#1692,#1683,#996,.T.);
#2097=EDGE_CURVE('',#1693,#1692,#997,.T.);
#2098=EDGE_CURVE('',#1681,#1693,#998,.T.);
#2099=EDGE_CURVE('',#1694,#1687,#999,.T.);
#2100=EDGE_CURVE('',#1694,#1695,#1000,.T.);
#2101=EDGE_CURVE('',#1685,#1695,#1001,.T.);
#2102=EDGE_CURVE('',#1693,#1696,#1002,.T.);
#2103=EDGE_CURVE('',#1696,#1697,#1003,.T.);
#2104=EDGE_CURVE('',#1697,#1688,#135,.T.);
#2105=EDGE_CURVE('',#1691,#1698,#136,.T.);
#2106=EDGE_CURVE('',#1698,#1699,#1004,.T.);
#2107=EDGE_CURVE('',#1699,#1694,#1005,.T.);
#2108=EDGE_CURVE('',#1700,#1701,#1006,.T.);
#2109=EDGE_CURVE('',#1701,#1702,#1007,.T.);
#2110=EDGE_CURVE('',#1702,#1703,#1008,.T.);
#2111=EDGE_CURVE('',#1703,#1704,#1009,.T.);
#2112=EDGE_CURVE('',#1704,#1705,#137,.T.);
#2113=EDGE_CURVE('',#1705,#1700,#1010,.T.);
#2114=EDGE_CURVE('',#1689,#1690,#1435,.T.);
#2115=EDGE_CURVE('',#1705,#1697,#1436,.F.);
#2116=EDGE_CURVE('',#1698,#1704,#1437,.F.);
#2117=EDGE_CURVE('',#1699,#1703,#1011,.T.);
#2118=EDGE_CURVE('',#1700,#1696,#1012,.T.);
#2119=EDGE_CURVE('',#1706,#1692,#1013,.T.);
#2120=EDGE_CURVE('',#1701,#1706,#1014,.T.);
#2121=EDGE_CURVE('',#1707,#1706,#1015,.T.);
#2122=EDGE_CURVE('',#1702,#1707,#1016,.T.);
#2123=EDGE_CURVE('',#1695,#1707,#1017,.T.);
#2864=ORIENTED_EDGE('',*,*,#2082,.F.);
#2865=ORIENTED_EDGE('',*,*,#2083,.F.);
#2866=ORIENTED_EDGE('',*,*,#2084,.F.);
#2867=ORIENTED_EDGE('',*,*,#2085,.F.);
#2868=ORIENTED_EDGE('',*,*,#2086,.F.);
#2869=ORIENTED_EDGE('',*,*,#2087,.F.);
#2870=ORIENTED_EDGE('',*,*,#2088,.F.);
#2871=ORIENTED_EDGE('',*,*,#2089,.F.);
#2872=ORIENTED_EDGE('',*,*,#2090,.F.);
#2873=ORIENTED_EDGE('',*,*,#2091,.F.);
#2874=ORIENTED_EDGE('',*,*,#2092,.F.);
#2875=ORIENTED_EDGE('',*,*,#2083,.T.);
#2876=ORIENTED_EDGE('',*,*,#2093,.F.);
#2877=ORIENTED_EDGE('',*,*,#2094,.F.);
#2878=ORIENTED_EDGE('',*,*,#2095,.F.);
#2879=ORIENTED_EDGE('',*,*,#2087,.T.);
#2880=ORIENTED_EDGE('',*,*,#2085,.T.);
#2881=ORIENTED_EDGE('',*,*,#2096,.F.);
#2882=ORIENTED_EDGE('',*,*,#2097,.F.);
#2883=ORIENTED_EDGE('',*,*,#2098,.F.);
#2884=ORIENTED_EDGE('',*,*,#2089,.T.);
#2885=ORIENTED_EDGE('',*,*,#2099,.F.);
#2886=ORIENTED_EDGE('',*,*,#2100,.T.);
#2887=ORIENTED_EDGE('',*,*,#2101,.F.);
#2888=ORIENTED_EDGE('',*,*,#2082,.T.);
#2889=ORIENTED_EDGE('',*,*,#2098,.T.);
#2890=ORIENTED_EDGE('',*,*,#2102,.T.);
#2891=ORIENTED_EDGE('',*,*,#2103,.T.);
#2892=ORIENTED_EDGE('',*,*,#2104,.T.);
#2893=ORIENTED_EDGE('',*,*,#2090,.T.);
#2894=ORIENTED_EDGE('',*,*,#2088,.T.);
#2895=ORIENTED_EDGE('',*,*,#2095,.T.);
#2896=ORIENTED_EDGE('',*,*,#2105,.T.);
#2897=ORIENTED_EDGE('',*,*,#2106,.T.);
#2898=ORIENTED_EDGE('',*,*,#2107,.T.);
#2899=ORIENTED_EDGE('',*,*,#2099,.T.);
#2900=ORIENTED_EDGE('',*,*,#2108,.T.);
#2901=ORIENTED_EDGE('',*,*,#2109,.T.);
#2902=ORIENTED_EDGE('',*,*,#2110,.T.);
#2903=ORIENTED_EDGE('',*,*,#2111,.T.);
#2904=ORIENTED_EDGE('',*,*,#2112,.T.);
#2905=ORIENTED_EDGE('',*,*,#2113,.T.);
#2906=ORIENTED_EDGE('',*,*,#2094,.T.);
#2907=ORIENTED_EDGE('',*,*,#2114,.F.);
#2908=ORIENTED_EDGE('',*,*,#2091,.T.);
#2909=ORIENTED_EDGE('',*,*,#2104,.F.);
#2910=ORIENTED_EDGE('',*,*,#2115,.F.);
#2911=ORIENTED_EDGE('',*,*,#2112,.F.);
#2912=ORIENTED_EDGE('',*,*,#2116,.F.);
#2913=ORIENTED_EDGE('',*,*,#2105,.F.);
#2914=ORIENTED_EDGE('',*,*,#2111,.F.);
#2915=ORIENTED_EDGE('',*,*,#2117,.F.);
#2916=ORIENTED_EDGE('',*,*,#2106,.F.);
#2917=ORIENTED_EDGE('',*,*,#2116,.T.);
#2918=ORIENTED_EDGE('',*,*,#2113,.F.);
#2919=ORIENTED_EDGE('',*,*,#2115,.T.);
#2920=ORIENTED_EDGE('',*,*,#2103,.F.);
#2921=ORIENTED_EDGE('',*,*,#2118,.F.);
#2922=ORIENTED_EDGE('',*,*,#2108,.F.);
#2923=ORIENTED_EDGE('',*,*,#2118,.T.);
#2924=ORIENTED_EDGE('',*,*,#2102,.F.);
#2925=ORIENTED_EDGE('',*,*,#2097,.T.);
#2926=ORIENTED_EDGE('',*,*,#2119,.F.);
#2927=ORIENTED_EDGE('',*,*,#2120,.F.);
#2928=ORIENTED_EDGE('',*,*,#2109,.F.);
#2929=ORIENTED_EDGE('',*,*,#2120,.T.);
#2930=ORIENTED_EDGE('',*,*,#2121,.F.);
#2931=ORIENTED_EDGE('',*,*,#2122,.F.);
#2932=ORIENTED_EDGE('',*,*,#2110,.F.);
#2933=ORIENTED_EDGE('',*,*,#2122,.T.);
#2934=ORIENTED_EDGE('',*,*,#2123,.F.);
#2935=ORIENTED_EDGE('',*,*,#2100,.F.);
#2936=ORIENTED_EDGE('',*,*,#2107,.F.);
#2937=ORIENTED_EDGE('',*,*,#2117,.T.);
#2938=ORIENTED_EDGE('',*,*,#2086,.T.);
#2939=ORIENTED_EDGE('',*,*,#2101,.T.);
#2940=ORIENTED_EDGE('',*,*,#2123,.T.);
#2941=ORIENTED_EDGE('',*,*,#2121,.T.);
#2942=ORIENTED_EDGE('',*,*,#2119,.T.);
#2943=ORIENTED_EDGE('',*,*,#2096,.T.);
#2944=ORIENTED_EDGE('',*,*,#2084,.T.);
#2945=ORIENTED_EDGE('',*,*,#2092,.T.);
#2946=ORIENTED_EDGE('',*,*,#2114,.T.);
#2947=ORIENTED_EDGE('',*,*,#2093,.T.);
#3026=CYLINDRICAL_SURFACE('',#3549,0.5);
#3027=CYLINDRICAL_SURFACE('',#3553,0.5);
#3028=CYLINDRICAL_SURFACE('',#3567,0.2117);
#3175=ADVANCED_FACE('',(#481),#3026,.F.);
#3176=ADVANCED_FACE('',(#482),#3027,.F.);
#3177=ADVANCED_FACE('',(#483),#314,.T.);
#3178=ADVANCED_FACE('',(#484),#315,.T.);
#3179=ADVANCED_FACE('',(#485),#316,.T.);
#3180=ADVANCED_FACE('',(#486),#317,.T.);
#3181=ADVANCED_FACE('',(#487),#318,.T.);
#3182=ADVANCED_FACE('',(#488),#319,.T.);
#3183=ADVANCED_FACE('',(#489),#320,.T.);
#3184=ADVANCED_FACE('',(#490),#3028,.F.);
#3185=ADVANCED_FACE('',(#491),#321,.F.);
#3186=ADVANCED_FACE('',(#492),#322,.F.);
#3187=ADVANCED_FACE('',(#493),#323,.T.);
#3188=ADVANCED_FACE('',(#494),#324,.T.);
#3189=ADVANCED_FACE('',(#495),#325,.T.);
#3190=ADVANCED_FACE('',(#496),#326,.T.);
#3214=CLOSED_SHELL('',(#3175,#3176,#3177,#3178,#3179,#3180,#3181,#3182,
#3183,#3184,#3185,#3186,#3187,#3188,#3189,#3190));
#3548=AXIS2_PLACEMENT_3D('',#5309,#4339,#4340);
#3549=AXIS2_PLACEMENT_3D('',#5310,#4341,#4342);
#3550=AXIS2_PLACEMENT_3D('',#5313,#4343,#4344);
#3551=AXIS2_PLACEMENT_3D('',#5315,#4345,#4346);
#3552=AXIS2_PLACEMENT_3D('',#5318,#4348,#4349);
#3553=AXIS2_PLACEMENT_3D('',#5319,#4350,#4351);
#3554=AXIS2_PLACEMENT_3D('',#5324,#4353,#4354);
#3555=AXIS2_PLACEMENT_3D('',#5326,#4355,#4356);
#3556=AXIS2_PLACEMENT_3D('',#5327,#4357,#4358);
#3557=AXIS2_PLACEMENT_3D('',#5328,#4359,#4360);
#3558=AXIS2_PLACEMENT_3D('',#5334,#4364,#4365);
#3559=AXIS2_PLACEMENT_3D('',#5340,#4369,#4370);
#3560=AXIS2_PLACEMENT_3D('',#5346,#4374,#4375);
#3561=AXIS2_PLACEMENT_3D('',#5352,#4379,#4380);
#3562=AXIS2_PLACEMENT_3D('',#5357,#4383,#4384);
#3563=AXIS2_PLACEMENT_3D('',#5358,#4385,#4386);
#3564=AXIS2_PLACEMENT_3D('',#5360,#4387,#4388);
#3565=AXIS2_PLACEMENT_3D('',#5364,#4391,#4392);
#3566=AXIS2_PLACEMENT_3D('',#5375,#4397,#4398);
#3567=AXIS2_PLACEMENT_3D('',#5377,#4400,#4401);
#3568=AXIS2_PLACEMENT_3D('',#5378,#4402,#4403);
#3569=AXIS2_PLACEMENT_3D('',#5379,#4404,#4405);
#3570=AXIS2_PLACEMENT_3D('',#5380,#4406,#4407);
#3571=AXIS2_PLACEMENT_3D('',#5381,#4408,#4409);
#3572=AXIS2_PLACEMENT_3D('',#5383,#4411,#4412);
#3573=AXIS2_PLACEMENT_3D('',#5385,#4414,#4415);
#3574=AXIS2_PLACEMENT_3D('',#5389,#4418,#4419);
#3575=AXIS2_PLACEMENT_3D('',#5393,#4422,#4423);
#3576=AXIS2_PLACEMENT_3D('',#5395,#4425,#4426);
#4339=DIRECTION('axis',(0.,0.,1.));
#4340=DIRECTION('refdir',(1.,0.,0.));
#4341=DIRECTION('center_axis',(0.,1.,0.));
#4342=DIRECTION('ref_axis',(1.,0.,0.));
#4343=DIRECTION('center_axis',(0.,-0.707106781186548,0.707106781186548));
#4344=DIRECTION('ref_axis',(0.,-0.707106781186547,-0.707106781186547));
#4345=DIRECTION('center_axis',(0.,1.,0.));
#4346=DIRECTION('ref_axis',(1.,0.,0.));
#4347=DIRECTION('',(0.,-1.,0.));
#4348=DIRECTION('center_axis',(0.,-1.,0.));
#4349=DIRECTION('ref_axis',(1.,0.,0.));
#4350=DIRECTION('center_axis',(0.,1.,0.));
#4351=DIRECTION('ref_axis',(1.,0.,0.));
#4352=DIRECTION('',(0.,1.,0.));
#4353=DIRECTION('center_axis',(0.,1.,0.));
#4354=DIRECTION('ref_axis',(1.,0.,0.));
#4355=DIRECTION('center_axis',(0.,-0.707106781186548,0.707106781186548));
#4356=DIRECTION('ref_axis',(0.,-0.707106781186547,-0.707106781186547));
#4357=DIRECTION('center_axis',(0.,-1.,0.));
#4358=DIRECTION('ref_axis',(1.,0.,0.));
#4359=DIRECTION('center_axis',(0.,1.,0.));
#4360=DIRECTION('ref_axis',(1.,0.,0.));
#4361=DIRECTION('',(1.,0.,0.));
#4362=DIRECTION('',(0.,0.,-1.));
#4363=DIRECTION('',(-1.,0.,0.));
#4364=DIRECTION('center_axis',(0.,1.,0.));
#4365=DIRECTION('ref_axis',(1.,0.,0.));
#4366=DIRECTION('',(-1.,0.,0.));
#4367=DIRECTION('',(0.,0.,1.));
#4368=DIRECTION('',(1.,0.,0.));
#4369=DIRECTION('center_axis',(0.,1.,0.));
#4370=DIRECTION('ref_axis',(-1.,0.,0.));
#4371=DIRECTION('',(-1.,0.,0.));
#4372=DIRECTION('',(0.,0.,1.));
#4373=DIRECTION('',(1.,0.,0.));
#4374=DIRECTION('center_axis',(0.,1.,0.));
#4375=DIRECTION('ref_axis',(-1.,0.,0.));
#4376=DIRECTION('',(1.,0.,0.));
#4377=DIRECTION('',(0.,0.,1.));
#4378=DIRECTION('',(-1.,0.,0.));
#4379=DIRECTION('center_axis',(0.,0.707106781186548,-0.707106781186548));
#4380=DIRECTION('ref_axis',(-1.,0.,0.));
#4381=DIRECTION('',(0.,-0.707106781186548,-0.707106781186548));
#4382=DIRECTION('',(-1.,0.,0.));
#4383=DIRECTION('center_axis',(0.,-0.707106781186548,0.707106781186548));
#4384=DIRECTION('ref_axis',(0.,0.707106781186547,0.707106781186547));
#4385=DIRECTION('center_axis',(0.,0.707106781186548,-0.707106781186548));
#4386=DIRECTION('ref_axis',(-1.,0.,0.));
#4387=DIRECTION('center_axis',(0.,-0.707106781186548,0.707106781186548));
#4388=DIRECTION('ref_axis',(0.,0.707106781186547,0.707106781186547));
#4389=DIRECTION('',(-1.,0.,0.));
#4390=DIRECTION('',(0.,0.707106781186548,0.707106781186548));
#4391=DIRECTION('center_axis',(0.,-0.707106781186548,-0.707106781186548));
#4392=DIRECTION('ref_axis',(-1.,0.,0.));
#4393=DIRECTION('',(0.,-0.707106781186548,0.707106781186548));
#4394=DIRECTION('',(-1.,0.,0.));
#4395=DIRECTION('',(0.,0.707106781186548,-0.707106781186548));
#4396=DIRECTION('',(1.,0.,0.));
#4397=DIRECTION('center_axis',(0.,0.707106781186548,0.707106781186548));
#4398=DIRECTION('ref_axis',(0.,0.707106781186547,-0.707106781186547));
#4399=DIRECTION('',(1.,0.,0.));
#4400=DIRECTION('center_axis',(0.,0.,1.));
#4401=DIRECTION('ref_axis',(-1.83697019872103E-16,-1.,0.));
#4402=DIRECTION('center_axis',(0.,0.,-1.));
#4403=DIRECTION('ref_axis',(1.,0.,0.));
#4404=DIRECTION('center_axis',(0.,0.,-1.));
#4405=DIRECTION('ref_axis',(1.,0.,0.));
#4406=DIRECTION('center_axis',(0.,0.,-1.));
#4407=DIRECTION('ref_axis',(1.,0.,0.));
#4408=DIRECTION('center_axis',(0.,0.,1.));
#4409=DIRECTION('ref_axis',(1.,0.,0.));
#4410=DIRECTION('',(0.,-1.,0.));
#4411=DIRECTION('center_axis',(0.,0.,1.));
#4412=DIRECTION('ref_axis',(1.,0.,0.));
#4413=DIRECTION('',(0.,1.,0.));
#4414=DIRECTION('center_axis',(1.,0.,0.));
#4415=DIRECTION('ref_axis',(0.,1.,0.));
#4416=DIRECTION('',(0.,1.,0.));
#4417=DIRECTION('',(0.,0.,1.));
#4418=DIRECTION('center_axis',(0.,-1.,0.));
#4419=DIRECTION('ref_axis',(1.,0.,0.));
#4420=DIRECTION('',(1.,0.,0.));
#4421=DIRECTION('',(0.,0.,1.));
#4422=DIRECTION('center_axis',(-1.,0.,0.));
#4423=DIRECTION('ref_axis',(0.,-1.,0.));
#4424=DIRECTION('',(0.,-1.,0.));
#4425=DIRECTION('center_axis',(0.,0.,1.));
#4426=DIRECTION('ref_axis',(1.,0.,0.));
#5309=CARTESIAN_POINT('',(0.,0.,0.));
#5310=CARTESIAN_POINT('Origin',(0.,0.2,0.));
#5311=CARTESIAN_POINT('',(0.49749371855331,0.2,0.05));
#5312=CARTESIAN_POINT('',(0.476969600708473,0.3,0.15));
#5313=CARTESIAN_POINT('Origin',(0.,0.15,0.));
#5314=CARTESIAN_POINT('',(0.3,0.2,0.4));
#5315=CARTESIAN_POINT('Origin',(0.,0.2,0.));
#5316=CARTESIAN_POINT('',(0.3,0.3,0.4));
#5317=CARTESIAN_POINT('',(0.3,0.2,0.4));
#5318=CARTESIAN_POINT('Origin',(0.,0.3,0.));
#5319=CARTESIAN_POINT('Origin',(0.,0.2,0.));
#5320=CARTESIAN_POINT('',(-0.3,0.2,0.4));
#5321=CARTESIAN_POINT('',(-0.3,0.3,0.4));
#5322=CARTESIAN_POINT('',(-0.3,0.2,0.4));
#5323=CARTESIAN_POINT('',(-0.49749371855331,0.2,0.05));
#5324=CARTESIAN_POINT('Origin',(0.,0.2,0.));
#5325=CARTESIAN_POINT('',(-0.476969600708473,0.3,0.15));
#5326=CARTESIAN_POINT('Origin',(0.,0.15,0.));
#5327=CARTESIAN_POINT('Origin',(0.,0.3,0.));
#5328=CARTESIAN_POINT('Origin',(0.,0.2,0.));
#5329=CARTESIAN_POINT('',(0.069403818338763,0.2,0.05));
#5330=CARTESIAN_POINT('',(0.125,0.2,0.05));
#5331=CARTESIAN_POINT('',(0.0694038183387628,0.2,0.4));
#5332=CARTESIAN_POINT('',(0.0694038183387628,0.2,-0.1));
#5333=CARTESIAN_POINT('',(0.,0.2,0.4));
#5334=CARTESIAN_POINT('Origin',(0.,0.2,0.));
#5335=CARTESIAN_POINT('',(-0.0694038183387628,0.2,0.4));
#5336=CARTESIAN_POINT('',(0.,0.2,0.4));
#5337=CARTESIAN_POINT('',(-0.069403818338763,0.2,0.05));
#5338=CARTESIAN_POINT('',(-0.0694038183387628,0.2,-0.1));
#5339=CARTESIAN_POINT('',(0.125,0.2,0.05));
#5340=CARTESIAN_POINT('Origin',(0.5,0.3,0.));
#5341=CARTESIAN_POINT('',(0.5,0.3,0.4));
#5342=CARTESIAN_POINT('',(0.5,0.3,0.4));
#5343=CARTESIAN_POINT('',(0.5,0.3,0.15));
#5344=CARTESIAN_POINT('',(0.5,0.3,0.));
#5345=CARTESIAN_POINT('',(0.25,0.3,0.15));
#5346=CARTESIAN_POINT('Origin',(0.5,0.3,0.));
#5347=CARTESIAN_POINT('',(-0.5,0.3,0.15));
#5348=CARTESIAN_POINT('',(0.25,0.3,0.15));
#5349=CARTESIAN_POINT('',(-0.5,0.3,0.4));
#5350=CARTESIAN_POINT('',(-0.5,0.3,0.));
#5351=CARTESIAN_POINT('',(0.5,0.3,0.4));
#5352=CARTESIAN_POINT('Origin',(0.25,0.225,0.075));
#5353=CARTESIAN_POINT('',(0.5,0.15,0.));
#5354=CARTESIAN_POINT('',(0.5,0.075,-0.075));
#5355=CARTESIAN_POINT('',(0.149388386429468,0.15,0.));
#5356=CARTESIAN_POINT('',(0.25,0.15,0.));
#5357=CARTESIAN_POINT('Origin',(0.,0.,-0.15));
#5358=CARTESIAN_POINT('Origin',(0.25,0.225,0.075));
#5359=CARTESIAN_POINT('',(-0.149388386429468,0.15,0.));
#5360=CARTESIAN_POINT('Origin',(0.,0.,-0.15));
#5361=CARTESIAN_POINT('',(-0.5,0.15,0.));
#5362=CARTESIAN_POINT('',(0.25,0.15,0.));
#5363=CARTESIAN_POINT('',(-0.5,0.225,0.075));
#5364=CARTESIAN_POINT('Origin',(-0.25,-0.225,0.075));
#5365=CARTESIAN_POINT('',(0.5,-0.15,0.));
#5366=CARTESIAN_POINT('',(0.5,-0.3,0.15));
#5367=CARTESIAN_POINT('',(0.5,-0.225,0.075));
#5368=CARTESIAN_POINT('',(-0.5,-0.3,0.15));
#5369=CARTESIAN_POINT('',(-0.25,-0.3,0.15));
#5370=CARTESIAN_POINT('',(-0.5,-0.15,0.));
#5371=CARTESIAN_POINT('',(-0.5,-0.075,-0.075));
#5372=CARTESIAN_POINT('',(-0.149388386429468,-0.15,0.));
#5373=CARTESIAN_POINT('',(-0.25,-0.15,0.));
#5374=CARTESIAN_POINT('',(0.149388386429468,-0.15,0.));
#5375=CARTESIAN_POINT('Origin',(0.,0.,-0.15));
#5376=CARTESIAN_POINT('',(-0.25,-0.15,0.));
#5377=CARTESIAN_POINT('Origin',(0.,0.,-0.1));
#5378=CARTESIAN_POINT('Origin',(0.,0.,0.4));
#5379=CARTESIAN_POINT('Origin',(0.,0.,0.));
#5380=CARTESIAN_POINT('Origin',(0.,0.,0.));
#5381=CARTESIAN_POINT('Origin',(0.,0.,0.));
#5382=CARTESIAN_POINT('',(-0.5,0.3,0.));
#5383=CARTESIAN_POINT('Origin',(0.,0.,0.));
#5384=CARTESIAN_POINT('',(0.5,-0.3,0.));
#5385=CARTESIAN_POINT('Origin',(0.5,-0.3,0.));
#5386=CARTESIAN_POINT('',(0.5,-0.3,0.4));
#5387=CARTESIAN_POINT('',(0.5,-0.3,0.4));
#5388=CARTESIAN_POINT('',(0.5,-0.3,0.));
#5389=CARTESIAN_POINT('Origin',(-0.5,-0.3,0.));
#5390=CARTESIAN_POINT('',(-0.5,-0.3,0.4));
#5391=CARTESIAN_POINT('',(-0.5,-0.3,0.4));
#5392=CARTESIAN_POINT('',(-0.5,-0.3,0.));
#5393=CARTESIAN_POINT('Origin',(-0.5,0.3,0.));
#5394=CARTESIAN_POINT('',(-0.5,0.3,0.4));
#5395=CARTESIAN_POINT('Origin',(0.,0.,0.4));
#5487=UNCERTAINTY_MEASURE_WITH_UNIT(LENGTH_MEASURE(0.001),#5503,
'DISTANCE_ACCURACY_VALUE',
'Maximum model space distance between geometric entities at asserted c
onnectivities');
#5489=UNCERTAINTY_MEASURE_WITH_UNIT(LENGTH_MEASURE(0.001),#5503,
'DISTANCE_ACCURACY_VALUE',
'Maximum model space distance between geometric entities at asserted c
onnectivities');
#5500=(
GEOMETRIC_REPRESENTATION_CONTEXT(3)
GLOBAL_UNCERTAINTY_ASSIGNED_CONTEXT((#5487))
GLOBAL_UNIT_ASSIGNED_CONTEXT((#5503,#5505,#5506))
REPRESENTATION_CONTEXT('','3D')
);
#5502=(
GEOMETRIC_REPRESENTATION_CONTEXT(3)
GLOBAL_UNCERTAINTY_ASSIGNED_CONTEXT((#5489))
GLOBAL_UNIT_ASSIGNED_CONTEXT((#5503,#5505,#5506))
REPRESENTATION_CONTEXT('','3D')
);
#5503=(
LENGTH_UNIT()
NAMED_UNIT(*)
SI_UNIT(.CENTI.,.METRE.)
);
#5505=(
NAMED_UNIT(*)
PLANE_ANGLE_UNIT()
SI_UNIT($,.RADIAN.)
);
#5506=(
NAMED_UNIT(*)
SI_UNIT($,.STERADIAN.)
SOLID_ANGLE_UNIT()
);
#5517=SHAPE_DEFINITION_REPRESENTATION(#5532,#5564);
#5532=PRODUCT_DEFINITION_SHAPE('',$,#5577);
#5564=SHAPE_REPRESENTATION('',(#3548),#5500);
#5566=PRODUCT_DEFINITION_CONTEXT('part definition',#5604,'design');
#5577=PRODUCT_DEFINITION('Slot Nut - M5 for 20 mm Extrusion',
'Slot Nut - M5 for 20 mm Extrusion',#5589,#5566);
#5589=PRODUCT_DEFINITION_FORMATION('',$,#5616);
#5604=APPLICATION_CONTEXT(
'Core Data for Automotive Mechanical Design Process');
#5605=PRODUCT_CONTEXT('part definition',#5604,'mechanical');
#5616=PRODUCT('Slot Nut - M5 for 20 mm Extrusion',
'Slot Nut - M5 for 20 mm Extrusion','Slot Nut - M5 for 20 mm Extrusion',
(#5605));
#5695=COLOUR_RGB('Black',0.12,0.14,0.17);
#5696=FILL_AREA_STYLE_COLOUR('',#5695);
#5697=FILL_AREA_STYLE('',(#5696));
#5698=SURFACE_STYLE_FILL_AREA(#5697);
#5699=SURFACE_SIDE_STYLE('',(#5698));
#5700=SURFACE_STYLE_USAGE(.BOTH.,#5699);
#5701=PRESENTATION_STYLE_ASSIGNMENT((#5700));
ENDSEC;
END-ISO-10303-21;
